ISO-10303-21;
HEADER;
/* Generated by software containing ST-Developer
 * from STEP Tools, Inc. (www.steptools.com) 
 */

FILE_DESCRIPTION(
/* description */ (''),
/* implementation_level */ '2;1');

FILE_NAME(
/* name */ 'Pin_02.step',
/* time_stamp */ '2026-09-20T21:58:27+06:00',
/* author */ (''),
/* organization */ (''),
/* preprocessor_version */ 'ST-DEVELOPER v20.2',
/* originating_system */ 'Autodesk Translation Framework v15.15.0.0',
/* authorisation */ '');

FILE_SCHEMA (('AUTOMOTIVE_DESIGN { 1 0 10303 214 3 1 1 }'));
ENDSEC;

DATA;
#10=MECHANICAL_DESIGN_GEOMETRIC_PRESENTATION_REPRESENTATION('',(#61),#2238);
#45=SHAPE_REPRESENTATION_RELATIONSHIP('SRR','None',#2272,#53);
#53=ADVANCED_BREP_SHAPE_REPRESENTATION('',(#69),#2232);
#61=STYLED_ITEM('',(#2321),#69);
#69=MANIFOLD_SOLID_BREP('Pin_02',#1208);
#105=PLANE('',#1401);
#106=PLANE('',#1405);
#163=FACE_OUTER_BOUND('',#234,.T.);
#164=FACE_OUTER_BOUND('',#235,.T.);
#165=FACE_OUTER_BOUND('',#236,.T.);
#234=EDGE_LOOP('',(#1010));
#235=EDGE_LOOP('',(#1011,#1012,#1013,#1014));
#236=EDGE_LOOP('',(#1015));
#335=LINE('',#2109,#420);
#420=VECTOR('',#1727,2.5);
#495=CIRCLE('',#1402,2.5);
#496=CIRCLE('',#1404,2.5);
#593=VERTEX_POINT('',#2105);
#594=VERTEX_POINT('',#2108);
#737=EDGE_CURVE('',#593,#593,#495,.T.);
#738=EDGE_CURVE('',#593,#594,#335,.T.);
#739=EDGE_CURVE('',#594,#594,#496,.T.);
#1010=ORIENTED_EDGE('',*,*,#737,.T.);
#1011=ORIENTED_EDGE('',*,*,#737,.F.);
#1012=ORIENTED_EDGE('',*,*,#738,.T.);
#1013=ORIENTED_EDGE('',*,*,#739,.T.);
#1014=ORIENTED_EDGE('',*,*,#738,.F.);
#1015=ORIENTED_EDGE('',*,*,#739,.F.);
#1126=CYLINDRICAL_SURFACE('',#1403,2.5);
#1179=ADVANCED_FACE('',(#163),#105,.T.);
#1180=ADVANCED_FACE('',(#164),#1126,.T.);
#1181=ADVANCED_FACE('',(#165),#106,.T.);
#1208=CLOSED_SHELL('',(#1179,#1180,#1181));
#1400=AXIS2_PLACEMENT_3D('',#2103,#1719,#1720);
#1401=AXIS2_PLACEMENT_3D('',#2104,#1721,#1722);
#1402=AXIS2_PLACEMENT_3D('',#2106,#1723,#1724);
#1403=AXIS2_PLACEMENT_3D('',#2107,#1725,#1726);
#1404=AXIS2_PLACEMENT_3D('',#2110,#1728,#1729);
#1405=AXIS2_PLACEMENT_3D('',#2111,#1730,#1731);
#1719=DIRECTION('axis',(0.,0.,1.));
#1720=DIRECTION('refdir',(1.,0.,0.));
#1721=DIRECTION('center_axis',(0.,-1.,0.));
#1722=DIRECTION('ref_axis',(1.,0.,0.));
#1723=DIRECTION('center_axis',(0.,-1.,0.));
#1724=DIRECTION('ref_axis',(1.,0.,0.));
#1725=DIRECTION('center_axis',(0.,-1.,0.));
#1726=DIRECTION('ref_axis',(1.,0.,0.));
#1727=DIRECTION('',(0.,1.,0.));
#1728=DIRECTION('center_axis',(0.,-1.,0.));
#1729=DIRECTION('ref_axis',(1.,0.,0.));
#1730=DIRECTION('center_axis',(0.,1.,0.));
#1731=DIRECTION('ref_axis',(0.,0.,1.));
#2103=CARTESIAN_POINT('',(0.,0.,0.));
#2104=CARTESIAN_POINT('Origin',(0.,-5.,64.2867316297599));
#2105=CARTESIAN_POINT('',(-2.5,-5.,64.2867316297599));
#2106=CARTESIAN_POINT('Origin',(0.,-5.,64.2867316297599));
#2107=CARTESIAN_POINT('Origin',(0.,3.,64.2867316297599));
#2108=CARTESIAN_POINT('',(-2.5,5.,64.2867316297599));
#2109=CARTESIAN_POINT('',(-2.5,3.,64.2867316297599));
#2110=CARTESIAN_POINT('Origin',(0.,5.,64.2867316297599));
#2111=CARTESIAN_POINT('Origin',(0.,5.,50.));
#2222=UNCERTAINTY_MEASURE_WITH_UNIT(LENGTH_MEASURE(0.01),#2239,
'DISTANCE_ACCURACY_VALUE',
'Maximum model space distance between geometric entities at asserted c
onnectivities');
#2228=UNCERTAINTY_MEASURE_WITH_UNIT(LENGTH_MEASURE(0.01),#2239,
'DISTANCE_ACCURACY_VALUE',
'Maximum model space distance between geometric entities at asserted c
onnectivities');
#2232=(
GEOMETRIC_REPRESENTATION_CONTEXT(3)
GLOBAL_UNCERTAINTY_ASSIGNED_CONTEXT((#2222))
GLOBAL_UNIT_ASSIGNED_CONTEXT((#2239,#2241,#2242))
REPRESENTATION_CONTEXT('','3D')
);
#2238=(
GEOMETRIC_REPRESENTATION_CONTEXT(3)
GLOBAL_UNCERTAINTY_ASSIGNED_CONTEXT((#2228))
GLOBAL_UNIT_ASSIGNED_CONTEXT((#2239,#2241,#2242))
REPRESENTATION_CONTEXT('','3D')
);
#2239=(
LENGTH_UNIT()
NAMED_UNIT(*)
SI_UNIT(.MILLI.,.METRE.)
);
#2241=(
NAMED_UNIT(*)
PLANE_ANGLE_UNIT()
SI_UNIT($,.RADIAN.)
);
#2242=(
NAMED_UNIT(*)
SI_UNIT($,.STERADIAN.)
SOLID_ANGLE_UNIT()
);
#2246=SHAPE_DEFINITION_REPRESENTATION(#2255,#2272);
#2255=PRODUCT_DEFINITION_SHAPE('',$,#2282);
#2272=SHAPE_REPRESENTATION('',(#1400),#2232);
#2278=PRODUCT_DEFINITION_CONTEXT('part definition',#2307,'design');
#2282=PRODUCT_DEFINITION('Pin_02','Pin_02',#2291,#2278);
#2291=PRODUCT_DEFINITION_FORMATION('',$,#2312);
#2307=APPLICATION_CONTEXT(
'Core Data for Automotive Mechanical Design Process');
#2308=PRODUCT_CONTEXT('part definition',#2307,'mechanical');
#2312=PRODUCT('Pin_02','Pin_02',$,(#2308));
#2321=PRESENTATION_STYLE_ASSIGNMENT((#2325));
#2325=SURFACE_STYLE_USAGE(.BOTH.,#2329);
#2329=SURFACE_SIDE_STYLE('',(#2333));
#2333=SURFACE_STYLE_FILL_AREA(#2337);
#2337=FILL_AREA_STYLE('Surface - Matte',(#2341));
#2341=FILL_AREA_STYLE_COLOUR('Surface - Matte',#2345);
#2345=COLOUR_RGB('Surface - Matte', 0.31764706, 0.68627451, 0.89019608);
ENDSEC;
END-ISO-10303-21;
